ISO-10303-21;
HEADER;
FILE_DESCRIPTION((''),'2;1');
FILE_NAME('Washer_4.step','2026-10-09T10:15:02-07:00',(''),(''),'','','');
FILE_SCHEMA (('AUTOMOTIVE_DESIGN { 1 0 10303 214 3 1 1 }'));
ENDSEC;
DATA;
#10=MECHANICAL_DESIGN_GEOMETRIC_PRESENTATION_REPRESENTATION('',(#88),#6779);
#68=SHAPE_REPRESENTATION_RELATIONSHIP('SRR','None',#6822,#78) ;
#78=ADVANCED_BREP_SHAPE_REPRESENTATION('',(#98),#6774) ;
#88=STYLED_ITEM('',(#6877),#98) ;
#98=MANIFOLD_SOLID_BREP('Body1',#3900) ;
#125=FACE_BOUND('',#776,.T.) ;
#126=FACE_BOUND('',#778,.T.) ;
#221=PLANE('',#4325) ;
#222=PLANE('',#4326) ;
#507=FACE_OUTER_BOUND('',#773,.T.) ;
#508=FACE_OUTER_BOUND('',#774,.T.) ;
#509=FACE_OUTER_BOUND('',#775,.T.) ;
#510=FACE_OUTER_BOUND('',#777,.T.) ;
#773=EDGE_LOOP('',(#3351,#3352,#3353,#3354)) ;
#774=EDGE_LOOP('',(#3355,#3356,#3357,#3358)) ;
#775=EDGE_LOOP('',(#3359)) ;
#776=EDGE_LOOP('',(#3360)) ;
#777=EDGE_LOOP('',(#3361)) ;
#778=EDGE_LOOP('',(#3362)) ;
#1121=LINE('',#6476,#1481) ;
#1122=LINE('',#6482,#1482) ;
#1481=VECTOR('',#5321,6.) ;
#1482=VECTOR('',#5328,3.2) ;
#1683=CIRCLE('',#4320,6.) ;
#1684=CIRCLE('',#4321,6.) ;
#1685=CIRCLE('',#4323,3.2) ;
#1686=CIRCLE('',#4324,3.2) ;
#1951=VERTEX_POINT('',#6473) ;
#1952=VERTEX_POINT('',#6475) ;
#1953=VERTEX_POINT('',#6479) ;
#1954=VERTEX_POINT('',#6481) ;
#2429=EDGE_CURVE('',#1951,#1951,#1683,.T.) ;
#2430=EDGE_CURVE('',#1951,#1952,#1121,.T.) ;
#2431=EDGE_CURVE('',#1952,#1952,#1684,.T.) ;
#2432=EDGE_CURVE('',#1953,#1953,#1685,.T.) ;
#2433=EDGE_CURVE('',#1953,#1954,#1122,.T.) ;
#2434=EDGE_CURVE('',#1954,#1954,#1686,.T.) ;
#3351=ORIENTED_EDGE('',*,*,#2429,.F.) ;
#3352=ORIENTED_EDGE('',*,*,#2430,.T.) ;
#3353=ORIENTED_EDGE('',*,*,#2431,.T.) ;
#3354=ORIENTED_EDGE('',*,*,#2430,.F.) ;
#3355=ORIENTED_EDGE('',*,*,#2432,.F.) ;
#3356=ORIENTED_EDGE('',*,*,#2433,.T.) ;
#3357=ORIENTED_EDGE('',*,*,#2434,.T.) ;
#3358=ORIENTED_EDGE('',*,*,#2433,.F.) ;
#3359=ORIENTED_EDGE('',*,*,#2431,.F.) ;
#3360=ORIENTED_EDGE('',*,*,#2432,.T.) ;
#3361=ORIENTED_EDGE('',*,*,#2429,.T.) ;
#3362=ORIENTED_EDGE('',*,*,#2434,.F.) ;
#3641=CYLINDRICAL_SURFACE('',#4319,6.) ;
#3642=CYLINDRICAL_SURFACE('',#4322,3.2) ;
#3831=ADVANCED_FACE('',(#507),#3641,.T.) ;
#3832=ADVANCED_FACE('',(#508),#3642,.F.) ;
#3833=ADVANCED_FACE('',(#509,#125),#221,.F.) ;
#3834=ADVANCED_FACE('',(#510,#126),#222,.T.) ;
#3900=CLOSED_SHELL('',(#3831,#3832,#3833,#3834)) ;
#4318=AXIS2_PLACEMENT_3D('',#6471,#5315,#5316) ;
#4319=AXIS2_PLACEMENT_3D('',#6472,#5317,#5318) ;
#4320=AXIS2_PLACEMENT_3D('',#6474,#5319,#5320) ;
#4321=AXIS2_PLACEMENT_3D('',#6477,#5322,#5323) ;
#4322=AXIS2_PLACEMENT_3D('',#6478,#5324,#5325) ;
#4323=AXIS2_PLACEMENT_3D('',#6480,#5326,#5327) ;
#4324=AXIS2_PLACEMENT_3D('',#6483,#5329,#5330) ;
#4325=AXIS2_PLACEMENT_3D('',#6484,#5331,#5332) ;
#4326=AXIS2_PLACEMENT_3D('',#6485,#5333,#5334) ;
#5315=DIRECTION('axis',(0.,0.,1.)) ;
#5316=DIRECTION('refdir',(1.,0.,0.)) ;
#5317=DIRECTION('center_axis',(0.,-1.,0.)) ;
#5318=DIRECTION('ref_axis',(1.,0.,0.)) ;
#5319=DIRECTION('center_axis',(0.,-1.,0.)) ;
#5320=DIRECTION('ref_axis',(0.,0.,1.)) ;
#5321=DIRECTION('',(0.,1.,0.)) ;
#5322=DIRECTION('center_axis',(0.,-1.,0.)) ;
#5323=DIRECTION('ref_axis',(0.,0.,1.)) ;
#5324=DIRECTION('center_axis',(0.,-1.,0.)) ;
#5325=DIRECTION('ref_axis',(1.,0.,0.)) ;
#5326=DIRECTION('center_axis',(0.,-1.,0.)) ;
#5327=DIRECTION('ref_axis',(0.,0.,1.)) ;
#5328=DIRECTION('',(0.,-1.,0.)) ;
#5329=DIRECTION('center_axis',(0.,-1.,0.)) ;
#5330=DIRECTION('ref_axis',(0.,0.,1.)) ;
#5331=DIRECTION('center_axis',(0.,-1.,0.)) ;
#5332=DIRECTION('ref_axis',(1.,0.,0.)) ;
#5333=DIRECTION('center_axis',(0.,-1.,0.)) ;
#5334=DIRECTION('ref_axis',(1.,0.,0.)) ;
#6471=CARTESIAN_POINT('',(0.,0.,0.)) ;
#6472=CARTESIAN_POINT('Origin',(35.,-19.5,-10.)) ;
#6473=CARTESIAN_POINT('',(29.,-20.,-10.)) ;
#6474=CARTESIAN_POINT('Origin',(35.,-20.,-10.)) ;
#6475=CARTESIAN_POINT('',(29.,-19.,-10.)) ;
#6476=CARTESIAN_POINT('',(29.,-19.5,-10.)) ;
#6477=CARTESIAN_POINT('Origin',(35.,-19.,-10.)) ;
#6478=CARTESIAN_POINT('Origin',(35.,-19.5,-10.)) ;
#6479=CARTESIAN_POINT('',(31.8,-19.,-10.)) ;
#6480=CARTESIAN_POINT('Origin',(35.,-19.,-10.)) ;
#6481=CARTESIAN_POINT('',(31.8,-20.,-10.)) ;
#6482=CARTESIAN_POINT('',(31.8,-19.5,-10.)) ;
#6483=CARTESIAN_POINT('Origin',(35.,-20.,-10.)) ;
#6484=CARTESIAN_POINT('Origin',(0.,-19.,0.)) ;
#6485=CARTESIAN_POINT('Origin',(0.,-20.,0.)) ;
#6762=UNCERTAINTY_MEASURE_WITH_UNIT(LENGTH_MEASURE(0.01),#6780,
'DISTANCE_ACCURACY_VALUE',
'Maximum model space distance between geometric entities at asserted c
onnectivities') ;
#6767=UNCERTAINTY_MEASURE_WITH_UNIT(LENGTH_MEASURE(0.01),#6780,
'DISTANCE_ACCURACY_VALUE',
'Maximum model space distance between geometric entities at asserted c
onnectivities') ;
#6774=(
GEOMETRIC_REPRESENTATION_CONTEXT(3)
GLOBAL_UNCERTAINTY_ASSIGNED_CONTEXT((#6762))
GLOBAL_UNIT_ASSIGNED_CONTEXT((#6780,#6782,#6783))
REPRESENTATION_CONTEXT('','3D')
) ;
#6779=(
GEOMETRIC_REPRESENTATION_CONTEXT(3)
GLOBAL_UNCERTAINTY_ASSIGNED_CONTEXT((#6767))
GLOBAL_UNIT_ASSIGNED_CONTEXT((#6780,#6782,#6783))
REPRESENTATION_CONTEXT('','3D')
) ;
#6780=(
LENGTH_UNIT()
NAMED_UNIT(*)
SI_UNIT(.MILLI.,.METRE.)
) ;
#6782=(
NAMED_UNIT(*)
PLANE_ANGLE_UNIT()
SI_UNIT($,.RADIAN.)
) ;
#6783=(
NAMED_UNIT(*)
SI_UNIT($,.STERADIAN.)
SOLID_ANGLE_UNIT()
) ;
#6790=SHAPE_DEFINITION_REPRESENTATION(#6801,#6822) ;
#6801=PRODUCT_DEFINITION_SHAPE('',$,#6834) ;
#6822=SHAPE_REPRESENTATION('',(#4318),#6774) ;
#6827=PRODUCT_DEFINITION_CONTEXT('part definition',#6862,'design') ;
#6834=PRODUCT_DEFINITION('Washer_4','Washer_4',#6845,#6827) ;
#6845=PRODUCT_DEFINITION_FORMATION('',$,#6870) ;
#6862=APPLICATION_CONTEXT(
'Core Data for Automotive Mechanical Design Process') ;
#6863=PRODUCT_CONTEXT('part definition',#6862,'mechanical') ;
#6870=PRODUCT('Washer_4','Washer_4',$,(#6863)) ;
#6877=PRESENTATION_STYLE_ASSIGNMENT((#6880)) ;
#6880=SURFACE_STYLE_USAGE(.BOTH.,#6883) ;
#6883=SURFACE_SIDE_STYLE('',(#6886)) ;
#6886=SURFACE_STYLE_FILL_AREA(#6889) ;
#6889=FILL_AREA_STYLE('Opaque(203,203,203)',(#6892)) ;
#6892=FILL_AREA_STYLE_COLOUR('Opaque(203,203,203)',#6895) ;
#6895=COLOUR_RGB('Opaque(203,203,203)', 0.31764706, 0.68627451, 0.89019608) ;
ENDSEC;
END-ISO-10303-21;
